ISO-10303-21;
HEADER;
/* Generated by software containing ST-Developer
 * from STEP Tools, Inc. (www.steptools.com) 
 */

FILE_DESCRIPTION(
/* description */ ('Two-stage gear reducer in split housing'),
/* implementation_level */ '2;1');

FILE_NAME(
/* name */ 'Cap Screw - M4x16.step',
/* time_stamp */ '2026-10-28T03:22:31-07:00',
/* author */ (''),
/* organization */ (''),
/* preprocessor_version */ 'ST-DEVELOPER v20.2',
/* originating_system */ 'Autodesk Translation Framework v15.17.0.0',
/* authorisation */ '');

FILE_SCHEMA (('AUTOMOTIVE_DESIGN { 1 0 10303 214 3 1 1 }'));
ENDSEC;

DATA;
#10=MECHANICAL_DESIGN_GEOMETRIC_PRESENTATION_REPRESENTATION('',(#1276),#73366);
#1112=CONICAL_SURFACE('',#17681,0.325,0.785398163397448);
#1113=CONICAL_SURFACE('',#17685,0.335,0.785398163397448);
#1114=CONICAL_SURFACE('',#17689,0.21,0.463647609000806);
#1115=CONICAL_SURFACE('',#17693,0.18,0.785398163397448);
#1119=ORIENTED_CLOSED_SHELL('',*,#16166,.F.);
#1121=BREP_WITH_VOIDS('Body1',#16165,(#1119));
#1149=SHAPE_REPRESENTATION_RELATIONSHIP('SRR','None',#73638,#1205);
#1205=ADVANCED_BREP_SHAPE_REPRESENTATION('',(#1121),#73334);
#1276=STYLED_ITEM('',(#73995),#1121);
#1537=FACE_BOUND('',#3480,.T.);
#1788=PLANE('',#17679);
#1789=PLANE('',#17687);
#1790=PLANE('',#17695);
#1791=PLANE('',#17696);
#1792=PLANE('',#17697);
#1793=PLANE('',#17698);
#1794=PLANE('',#17699);
#1795=PLANE('',#17700);
#1796=PLANE('',#17701);
#1797=PLANE('',#17702);
#1798=PLANE('',#17703);
#2399=FACE_OUTER_BOUND('',#3475,.T.);
#2400=FACE_OUTER_BOUND('',#3476,.T.);
#2401=FACE_OUTER_BOUND('',#3477,.T.);
#2402=FACE_OUTER_BOUND('',#3478,.T.);
#2403=FACE_OUTER_BOUND('',#3479,.T.);
#2404=FACE_OUTER_BOUND('',#3481,.T.);
#2405=FACE_OUTER_BOUND('',#3482,.T.);
#2406=FACE_OUTER_BOUND('',#3483,.T.);
#2407=FACE_OUTER_BOUND('',#3484,.T.);
#2408=FACE_OUTER_BOUND('',#3485,.T.);
#2409=FACE_OUTER_BOUND('',#3486,.T.);
#2410=FACE_OUTER_BOUND('',#3487,.T.);
#2411=FACE_OUTER_BOUND('',#3488,.T.);
#2412=FACE_OUTER_BOUND('',#3489,.T.);
#2413=FACE_OUTER_BOUND('',#3490,.T.);
#2414=FACE_OUTER_BOUND('',#3491,.T.);
#2415=FACE_OUTER_BOUND('',#3492,.T.);
#3475=EDGE_LOOP('',(#12225));
#3476=EDGE_LOOP('',(#12226,#12227,#12228,#12229));
#3477=EDGE_LOOP('',(#12230,#12231,#12232,#12233));
#3478=EDGE_LOOP('',(#12234,#12235,#12236,#12237));
#3479=EDGE_LOOP('',(#12238));
#3480=EDGE_LOOP('',(#12239));
#3481=EDGE_LOOP('',(#12240,#12241,#12242,#12243));
#3482=EDGE_LOOP('',(#12244,#12245,#12246,#12247));
#3483=EDGE_LOOP('',(#12248,#12249,#12250,#12251));
#3484=EDGE_LOOP('',(#12252));
#3485=EDGE_LOOP('',(#12253,#12254,#12255,#12256));
#3486=EDGE_LOOP('',(#12257,#12258,#12259,#12260));
#3487=EDGE_LOOP('',(#12261,#12262,#12263,#12264));
#3488=EDGE_LOOP('',(#12265,#12266,#12267,#12268));
#3489=EDGE_LOOP('',(#12269,#12270,#12271,#12272));
#3490=EDGE_LOOP('',(#12273,#12274,#12275,#12276));
#3491=EDGE_LOOP('',(#12277,#12278,#12279,#12280,#12281,#12282));
#3492=EDGE_LOOP('',(#12283,#12284,#12285,#12286,#12287,#12288));
#4455=LINE('',#25299,#5479);
#4456=LINE('',#25303,#5480);
#4457=LINE('',#25307,#5481);
#4458=LINE('',#25314,#5482);
#4459=LINE('',#25318,#5483);
#4460=LINE('',#25322,#5484);
#4461=LINE('',#25327,#5485);
#4462=LINE('',#25329,#5486);
#4463=LINE('',#25331,#5487);
#4464=LINE('',#25332,#5488);
#4465=LINE('',#25335,#5489);
#4466=LINE('',#25337,#5490);
#4467=LINE('',#25338,#5491);
#4468=LINE('',#25341,#5492);
#4469=LINE('',#25343,#5493);
#4470=LINE('',#25344,#5494);
#4471=LINE('',#25347,#5495);
#4472=LINE('',#25349,#5496);
#4473=LINE('',#25350,#5497);
#4474=LINE('',#25353,#5498);
#4475=LINE('',#25355,#5499);
#4476=LINE('',#25356,#5500);
#4477=LINE('',#25358,#5501);
#4478=LINE('',#25359,#5502);
#5479=VECTOR('',#20599,0.325);
#5480=VECTOR('',#20604,0.35);
#5481=VECTOR('',#20609,0.335);
#5482=VECTOR('',#20618,0.21);
#5483=VECTOR('',#20623,0.2);
#5484=VECTOR('',#20628,0.18);
#5485=VECTOR('',#20633,1.);
#5486=VECTOR('',#20634,1.);
#5487=VECTOR('',#20635,1.);
#5488=VECTOR('',#20636,1.);
#5489=VECTOR('',#20639,1.);
#5490=VECTOR('',#20640,1.);
#5491=VECTOR('',#20641,1.);
#5492=VECTOR('',#20644,1.);
#5493=VECTOR('',#20645,1.);
#5494=VECTOR('',#20646,1.);
#5495=VECTOR('',#20649,1.);
#5496=VECTOR('',#20650,1.);
#5497=VECTOR('',#20651,1.);
#5498=VECTOR('',#20654,1.);
#5499=VECTOR('',#20655,1.);
#5500=VECTOR('',#20656,1.);
#5501=VECTOR('',#20659,1.);
#5502=VECTOR('',#20660,1.);
#6532=CIRCLE('',#17680,0.3);
#6533=CIRCLE('',#17682,0.35);
#6534=CIRCLE('',#17684,0.35);
#6535=CIRCLE('',#17686,0.32);
#6536=CIRCLE('',#17688,0.22);
#6537=CIRCLE('',#17690,0.1954);
#6538=CIRCLE('',#17692,0.1954);
#6539=CIRCLE('',#17694,0.16);
#7413=VERTEX_POINT('',#25294);
#7414=VERTEX_POINT('',#25297);
#7415=VERTEX_POINT('',#25301);
#7416=VERTEX_POINT('',#25305);
#7417=VERTEX_POINT('',#25309);
#7418=VERTEX_POINT('',#25312);
#7419=VERTEX_POINT('',#25316);
#7420=VERTEX_POINT('',#25320);
#7421=VERTEX_POINT('',#25325);
#7422=VERTEX_POINT('',#25326);
#7423=VERTEX_POINT('',#25328);
#7424=VERTEX_POINT('',#25330);
#7425=VERTEX_POINT('',#25334);
#7426=VERTEX_POINT('',#25336);
#7427=VERTEX_POINT('',#25340);
#7428=VERTEX_POINT('',#25342);
#7429=VERTEX_POINT('',#25346);
#7430=VERTEX_POINT('',#25348);
#7431=VERTEX_POINT('',#25352);
#7432=VERTEX_POINT('',#25354);
#9166=EDGE_CURVE('',#7413,#7413,#6532,.T.);
#9167=EDGE_CURVE('',#7414,#7414,#6533,.T.);
#9168=EDGE_CURVE('',#7414,#7413,#4455,.T.);
#9169=EDGE_CURVE('',#7415,#7415,#6534,.T.);
#9170=EDGE_CURVE('',#7415,#7414,#4456,.T.);
#9171=EDGE_CURVE('',#7416,#7416,#6535,.T.);
#9172=EDGE_CURVE('',#7416,#7415,#4457,.T.);
#9173=EDGE_CURVE('',#7417,#7417,#6536,.T.);
#9174=EDGE_CURVE('',#7418,#7418,#6537,.F.);
#9175=EDGE_CURVE('',#7418,#7417,#4458,.T.);
#9176=EDGE_CURVE('',#7419,#7419,#6538,.F.);
#9177=EDGE_CURVE('',#7419,#7418,#4459,.T.);
#9178=EDGE_CURVE('',#7420,#7420,#6539,.T.);
#9179=EDGE_CURVE('',#7420,#7419,#4460,.T.);
#9180=EDGE_CURVE('',#7421,#7422,#4461,.T.);
#9181=EDGE_CURVE('',#7422,#7423,#4462,.T.);
#9182=EDGE_CURVE('',#7423,#7424,#4463,.T.);
#9183=EDGE_CURVE('',#7421,#7424,#4464,.T.);
#9184=EDGE_CURVE('',#7422,#7425,#4465,.T.);
#9185=EDGE_CURVE('',#7425,#7426,#4466,.T.);
#9186=EDGE_CURVE('',#7426,#7423,#4467,.T.);
#9187=EDGE_CURVE('',#7425,#7427,#4468,.T.);
#9188=EDGE_CURVE('',#7427,#7428,#4469,.T.);
#9189=EDGE_CURVE('',#7428,#7426,#4470,.T.);
#9190=EDGE_CURVE('',#7427,#7429,#4471,.T.);
#9191=EDGE_CURVE('',#7429,#7430,#4472,.T.);
#9192=EDGE_CURVE('',#7430,#7428,#4473,.T.);
#9193=EDGE_CURVE('',#7429,#7431,#4474,.T.);
#9194=EDGE_CURVE('',#7431,#7432,#4475,.T.);
#9195=EDGE_CURVE('',#7432,#7430,#4476,.T.);
#9196=EDGE_CURVE('',#7431,#7421,#4477,.T.);
#9197=EDGE_CURVE('',#7424,#7432,#4478,.T.);
#12225=ORIENTED_EDGE('',*,*,#9166,.F.);
#12226=ORIENTED_EDGE('',*,*,#9167,.F.);
#12227=ORIENTED_EDGE('',*,*,#9168,.T.);
#12228=ORIENTED_EDGE('',*,*,#9166,.T.);
#12229=ORIENTED_EDGE('',*,*,#9168,.F.);
#12230=ORIENTED_EDGE('',*,*,#9169,.F.);
#12231=ORIENTED_EDGE('',*,*,#9170,.T.);
#12232=ORIENTED_EDGE('',*,*,#9167,.T.);
#12233=ORIENTED_EDGE('',*,*,#9170,.F.);
#12234=ORIENTED_EDGE('',*,*,#9171,.F.);
#12235=ORIENTED_EDGE('',*,*,#9172,.T.);
#12236=ORIENTED_EDGE('',*,*,#9169,.T.);
#12237=ORIENTED_EDGE('',*,*,#9172,.F.);
#12238=ORIENTED_EDGE('',*,*,#9171,.T.);
#12239=ORIENTED_EDGE('',*,*,#9173,.F.);
#12240=ORIENTED_EDGE('',*,*,#9174,.F.);
#12241=ORIENTED_EDGE('',*,*,#9175,.T.);
#12242=ORIENTED_EDGE('',*,*,#9173,.T.);
#12243=ORIENTED_EDGE('',*,*,#9175,.F.);
#12244=ORIENTED_EDGE('',*,*,#9176,.F.);
#12245=ORIENTED_EDGE('',*,*,#9177,.T.);
#12246=ORIENTED_EDGE('',*,*,#9174,.T.);
#12247=ORIENTED_EDGE('',*,*,#9177,.F.);
#12248=ORIENTED_EDGE('',*,*,#9178,.F.);
#12249=ORIENTED_EDGE('',*,*,#9179,.T.);
#12250=ORIENTED_EDGE('',*,*,#9176,.T.);
#12251=ORIENTED_EDGE('',*,*,#9179,.F.);
#12252=ORIENTED_EDGE('',*,*,#9178,.T.);
#12253=ORIENTED_EDGE('',*,*,#9180,.T.);
#12254=ORIENTED_EDGE('',*,*,#9181,.T.);
#12255=ORIENTED_EDGE('',*,*,#9182,.T.);
#12256=ORIENTED_EDGE('',*,*,#9183,.F.);
#12257=ORIENTED_EDGE('',*,*,#9184,.T.);
#12258=ORIENTED_EDGE('',*,*,#9185,.T.);
#12259=ORIENTED_EDGE('',*,*,#9186,.T.);
#12260=ORIENTED_EDGE('',*,*,#9181,.F.);
#12261=ORIENTED_EDGE('',*,*,#9187,.T.);
#12262=ORIENTED_EDGE('',*,*,#9188,.T.);
#12263=ORIENTED_EDGE('',*,*,#9189,.T.);
#12264=ORIENTED_EDGE('',*,*,#9185,.F.);
#12265=ORIENTED_EDGE('',*,*,#9190,.T.);
#12266=ORIENTED_EDGE('',*,*,#9191,.T.);
#12267=ORIENTED_EDGE('',*,*,#9192,.T.);
#12268=ORIENTED_EDGE('',*,*,#9188,.F.);
#12269=ORIENTED_EDGE('',*,*,#9193,.T.);
#12270=ORIENTED_EDGE('',*,*,#9194,.T.);
#12271=ORIENTED_EDGE('',*,*,#9195,.T.);
#12272=ORIENTED_EDGE('',*,*,#9191,.F.);
#12273=ORIENTED_EDGE('',*,*,#9196,.T.);
#12274=ORIENTED_EDGE('',*,*,#9183,.T.);
#12275=ORIENTED_EDGE('',*,*,#9197,.T.);
#12276=ORIENTED_EDGE('',*,*,#9194,.F.);
#12277=ORIENTED_EDGE('',*,*,#9196,.F.);
#12278=ORIENTED_EDGE('',*,*,#9193,.F.);
#12279=ORIENTED_EDGE('',*,*,#9190,.F.);
#12280=ORIENTED_EDGE('',*,*,#9187,.F.);
#12281=ORIENTED_EDGE('',*,*,#9184,.F.);
#12282=ORIENTED_EDGE('',*,*,#9180,.F.);
#12283=ORIENTED_EDGE('',*,*,#9197,.F.);
#12284=ORIENTED_EDGE('',*,*,#9182,.F.);
#12285=ORIENTED_EDGE('',*,*,#9186,.F.);
#12286=ORIENTED_EDGE('',*,*,#9189,.F.);
#12287=ORIENTED_EDGE('',*,*,#9192,.F.);
#12288=ORIENTED_EDGE('',*,*,#9195,.F.);
#15073=CYLINDRICAL_SURFACE('',#17683,0.35);
#15074=CYLINDRICAL_SURFACE('',#17691,0.1954);
#15606=ADVANCED_FACE('',(#2399),#1788,.T.);
#15607=ADVANCED_FACE('',(#2400),#1112,.T.);
#15608=ADVANCED_FACE('',(#2401),#15073,.T.);
#15609=ADVANCED_FACE('',(#2402),#1113,.T.);
#15610=ADVANCED_FACE('',(#2403,#1537),#1789,.T.);
#15611=ADVANCED_FACE('',(#2404),#1114,.T.);
#15612=ADVANCED_FACE('',(#2405),#15074,.T.);
#15613=ADVANCED_FACE('',(#2406),#1115,.T.);
#15614=ADVANCED_FACE('',(#2407),#1790,.T.);
#15615=ADVANCED_FACE('',(#2408),#1791,.F.);
#15616=ADVANCED_FACE('',(#2409),#1792,.F.);
#15617=ADVANCED_FACE('',(#2410),#1793,.F.);
#15618=ADVANCED_FACE('',(#2411),#1794,.F.);
#15619=ADVANCED_FACE('',(#2412),#1795,.F.);
#15620=ADVANCED_FACE('',(#2413),#1796,.F.);
#15621=ADVANCED_FACE('',(#2414),#1797,.F.);
#15622=ADVANCED_FACE('',(#2415),#1798,.F.);
#16165=CLOSED_SHELL('',(#15606,#15607,#15608,#15609,#15610,#15611,#15612,
#15613,#15614));
#16166=CLOSED_SHELL('',(#15615,#15616,#15617,#15618,#15619,#15620,#15621,
#15622));
#17678=AXIS2_PLACEMENT_3D('',#25292,#20589,#20590);
#17679=AXIS2_PLACEMENT_3D('',#25293,#20591,#20592);
#17680=AXIS2_PLACEMENT_3D('',#25295,#20593,#20594);
#17681=AXIS2_PLACEMENT_3D('',#25296,#20595,#20596);
#17682=AXIS2_PLACEMENT_3D('',#25298,#20597,#20598);
#17683=AXIS2_PLACEMENT_3D('',#25300,#20600,#20601);
#17684=AXIS2_PLACEMENT_3D('',#25302,#20602,#20603);
#17685=AXIS2_PLACEMENT_3D('',#25304,#20605,#20606);
#17686=AXIS2_PLACEMENT_3D('',#25306,#20607,#20608);
#17687=AXIS2_PLACEMENT_3D('',#25308,#20610,#20611);
#17688=AXIS2_PLACEMENT_3D('',#25310,#20612,#20613);
#17689=AXIS2_PLACEMENT_3D('',#25311,#20614,#20615);
#17690=AXIS2_PLACEMENT_3D('',#25313,#20616,#20617);
#17691=AXIS2_PLACEMENT_3D('',#25315,#20619,#20620);
#17692=AXIS2_PLACEMENT_3D('',#25317,#20621,#20622);
#17693=AXIS2_PLACEMENT_3D('',#25319,#20624,#20625);
#17694=AXIS2_PLACEMENT_3D('',#25321,#20626,#20627);
#17695=AXIS2_PLACEMENT_3D('',#25323,#20629,#20630);
#17696=AXIS2_PLACEMENT_3D('',#25324,#20631,#20632);
#17697=AXIS2_PLACEMENT_3D('',#25333,#20637,#20638);
#17698=AXIS2_PLACEMENT_3D('',#25339,#20642,#20643);
#17699=AXIS2_PLACEMENT_3D('',#25345,#20647,#20648);
#17700=AXIS2_PLACEMENT_3D('',#25351,#20652,#20653);
#17701=AXIS2_PLACEMENT_3D('',#25357,#20657,#20658);
#17702=AXIS2_PLACEMENT_3D('',#25360,#20661,#20662);
#17703=AXIS2_PLACEMENT_3D('',#25361,#20663,#20664);
#20589=DIRECTION('axis',(0.,0.,1.));
#20590=DIRECTION('refdir',(1.,0.,0.));
#20591=DIRECTION('center_axis',(0.,1.,0.));
#20592=DIRECTION('ref_axis',(0.,0.,1.));
#20593=DIRECTION('center_axis',(0.,-1.,0.));
#20594=DIRECTION('ref_axis',(1.,0.,0.));
#20595=DIRECTION('center_axis',(0.,-1.,0.));
#20596=DIRECTION('ref_axis',(1.,0.,0.));
#20597=DIRECTION('center_axis',(0.,-1.,0.));
#20598=DIRECTION('ref_axis',(1.,0.,0.));
#20599=DIRECTION('',(0.707106781186547,0.707106781186548,8.65956056235493E-17));
#20600=DIRECTION('center_axis',(0.,-1.,0.));
#20601=DIRECTION('ref_axis',(1.,0.,0.));
#20602=DIRECTION('center_axis',(0.,-1.,0.));
#20603=DIRECTION('ref_axis',(1.,0.,0.));
#20604=DIRECTION('',(0.,1.,0.));
#20605=DIRECTION('center_axis',(0.,1.,0.));
#20606=DIRECTION('ref_axis',(1.,0.,0.));
#20607=DIRECTION('center_axis',(0.,-1.,0.));
#20608=DIRECTION('ref_axis',(1.,0.,0.));
#20609=DIRECTION('',(-0.707106781186547,0.707106781186548,-8.65956056235493E-17));
#20610=DIRECTION('center_axis',(0.,-1.,0.));
#20611=DIRECTION('ref_axis',(0.,0.,-1.));
#20612=DIRECTION('center_axis',(0.,-1.,0.));
#20613=DIRECTION('ref_axis',(1.,0.,0.));
#20614=DIRECTION('center_axis',(0.,1.,0.));
#20615=DIRECTION('ref_axis',(1.,0.,0.));
#20616=DIRECTION('center_axis',(0.,1.,0.));
#20617=DIRECTION('ref_axis',(1.,0.,0.));
#20618=DIRECTION('',(-0.447213595499958,0.894427190999916,-5.47678698264203E-17));
#20619=DIRECTION('center_axis',(0.,-1.,0.));
#20620=DIRECTION('ref_axis',(1.,0.,0.));
#20621=DIRECTION('center_axis',(0.,1.,0.));
#20622=DIRECTION('ref_axis',(1.,0.,0.));
#20623=DIRECTION('',(0.,1.,0.));
#20624=DIRECTION('center_axis',(0.,1.,0.));
#20625=DIRECTION('ref_axis',(1.,0.,0.));
#20626=DIRECTION('center_axis',(0.,-1.,0.));
#20627=DIRECTION('ref_axis',(1.,0.,0.));
#20628=DIRECTION('',(-0.707106781186547,0.707106781186548,-8.65956056235493E-17));
#20629=DIRECTION('center_axis',(0.,-1.,0.));
#20630=DIRECTION('ref_axis',(0.,0.,-1.));
#20631=DIRECTION('center_axis',(0.866025403784439,0.,-0.5));
#20632=DIRECTION('ref_axis',(0.5,0.,0.866025403784439));
#20633=DIRECTION('',(-0.5,0.,-0.866025403784439));
#20634=DIRECTION('',(0.,-1.,0.));
#20635=DIRECTION('',(0.5,0.,0.866025403784439));
#20636=DIRECTION('',(0.,-1.,0.));
#20637=DIRECTION('center_axis',(1.60246890531964E-16,0.,-1.));
#20638=DIRECTION('ref_axis',(1.,0.,1.60246890531964E-16));
#20639=DIRECTION('',(-1.,0.,-1.60246890531964E-16));
#20640=DIRECTION('',(0.,-1.,0.));
#20641=DIRECTION('',(1.,0.,1.60246890531964E-16));
#20642=DIRECTION('center_axis',(-0.866025403784439,0.,-0.5));
#20643=DIRECTION('ref_axis',(0.5,0.,-0.866025403784439));
#20644=DIRECTION('',(-0.5,0.,0.866025403784439));
#20645=DIRECTION('',(0.,-1.,0.));
#20646=DIRECTION('',(0.5,0.,-0.866025403784439));
#20647=DIRECTION('center_axis',(-0.866025403784439,0.,0.5));
#20648=DIRECTION('ref_axis',(-0.5,0.,-0.866025403784439));
#20649=DIRECTION('',(0.5,0.,0.866025403784439));
#20650=DIRECTION('',(0.,-1.,0.));
#20651=DIRECTION('',(-0.5,0.,-0.866025403784439));
#20652=DIRECTION('center_axis',(-1.60246890531964E-16,0.,1.));
#20653=DIRECTION('ref_axis',(-1.,0.,-1.60246890531964E-16));
#20654=DIRECTION('',(1.,0.,1.60246890531964E-16));
#20655=DIRECTION('',(0.,-1.,0.));
#20656=DIRECTION('',(-1.,0.,-1.60246890531964E-16));
#20657=DIRECTION('center_axis',(0.866025403784439,0.,0.5));
#20658=DIRECTION('ref_axis',(-0.5,0.,0.866025403784439));
#20659=DIRECTION('',(0.5,0.,-0.866025403784439));
#20660=DIRECTION('',(-0.5,0.,0.866025403784439));
#20661=DIRECTION('center_axis',(0.,1.,0.));
#20662=DIRECTION('ref_axis',(1.,0.,0.));
#20663=DIRECTION('center_axis',(0.,-1.,0.));
#20664=DIRECTION('ref_axis',(0.,0.,-1.));
#25292=CARTESIAN_POINT('',(0.,0.,0.));
#25293=CARTESIAN_POINT('Origin',(0.3,0.4,0.));
#25294=CARTESIAN_POINT('',(-0.3,0.4,-3.67394039744206E-17));
#25295=CARTESIAN_POINT('Origin',(0.,0.4,0.));
#25296=CARTESIAN_POINT('Origin',(0.,0.375,0.));
#25297=CARTESIAN_POINT('',(-0.35,0.35,-4.28626379701573E-17));
#25298=CARTESIAN_POINT('Origin',(0.,0.35,0.));
#25299=CARTESIAN_POINT('',(-0.325,0.375,-3.9801020972289E-17));
#25300=CARTESIAN_POINT('Origin',(0.,0.19,0.));
#25301=CARTESIAN_POINT('',(-0.35,0.03,-4.28626379701574E-17));
#25302=CARTESIAN_POINT('Origin',(0.,0.03,0.));
#25303=CARTESIAN_POINT('',(-0.35,0.19,-4.28626379701574E-17));
#25304=CARTESIAN_POINT('Origin',(0.,0.0149999999999999,0.));
#25305=CARTESIAN_POINT('',(-0.32,-3.29597460435593E-17,-3.91886975727153E-17));
#25306=CARTESIAN_POINT('Origin',(0.,0.,0.));
#25307=CARTESIAN_POINT('',(-0.335,0.0149999999999999,-4.10256677714363E-17));
#25308=CARTESIAN_POINT('Origin',(0.22,0.,0.));
#25309=CARTESIAN_POINT('',(-0.22,-6.93889390390723E-18,-2.69422295812418E-17));
#25310=CARTESIAN_POINT('Origin',(0.,0.,0.));
#25311=CARTESIAN_POINT('Origin',(0.,-0.02,0.));
#25312=CARTESIAN_POINT('',(-0.1954,-0.0492,2.39295984553393E-17));
#25313=CARTESIAN_POINT('Origin',(0.,-0.0492,0.));
#25314=CARTESIAN_POINT('',(-0.21,-0.02,-2.57175827820944E-17));
#25315=CARTESIAN_POINT('Origin',(0.,-0.8,0.));
#25316=CARTESIAN_POINT('',(-0.1954,-1.5646,2.39295984553393E-17));
#25317=CARTESIAN_POINT('Origin',(0.,-1.5646,0.));
#25318=CARTESIAN_POINT('',(-0.1954,-0.8,-2.39295984553393E-17));
#25319=CARTESIAN_POINT('Origin',(0.,-1.58,0.));
#25320=CARTESIAN_POINT('',(-0.16,-1.6,-1.95943487863577E-17));
#25321=CARTESIAN_POINT('Origin',(0.,-1.6,0.));
#25322=CARTESIAN_POINT('',(-0.18,-1.58,-2.20436423846524E-17));
#25323=CARTESIAN_POINT('Origin',(0.,-1.6,0.));
#25324=CARTESIAN_POINT('Origin',(0.0866025403784439,-0.4,-0.15));
#25325=CARTESIAN_POINT('',(0.173205080756888,-0.4,0.));
#25326=CARTESIAN_POINT('',(0.0866025403784439,-0.4,-0.15));
#25327=CARTESIAN_POINT('',(0.173205080756888,-0.4,0.));
#25328=CARTESIAN_POINT('',(0.0866025403784439,-0.64,-0.15));
#25329=CARTESIAN_POINT('',(0.0866025403784439,-0.4,-0.15));
#25330=CARTESIAN_POINT('',(0.173205080756888,-0.64,0.));
#25331=CARTESIAN_POINT('',(0.173205080756888,-0.64,0.));
#25332=CARTESIAN_POINT('',(0.173205080756888,-0.4,0.));
#25333=CARTESIAN_POINT('Origin',(-0.0866025403784438,-0.4,-0.15));
#25334=CARTESIAN_POINT('',(-0.0866025403784438,-0.4,-0.15));
#25335=CARTESIAN_POINT('',(0.0866025403784439,-0.4,-0.15));
#25336=CARTESIAN_POINT('',(-0.0866025403784438,-0.64,-0.15));
#25337=CARTESIAN_POINT('',(-0.0866025403784438,-0.4,-0.15));
#25338=CARTESIAN_POINT('',(0.0866025403784439,-0.64,-0.15));
#25339=CARTESIAN_POINT('Origin',(-0.173205080756888,-0.4,-2.77555756156289E-17));
#25340=CARTESIAN_POINT('',(-0.173205080756888,-0.4,-2.12115047744981E-17));
#25341=CARTESIAN_POINT('',(-0.0866025403784438,-0.4,-0.15));
#25342=CARTESIAN_POINT('',(-0.173205080756888,-0.64,-2.77555756156289E-17));
#25343=CARTESIAN_POINT('',(-0.173205080756888,-0.4,-2.12115047744981E-17));
#25344=CARTESIAN_POINT('',(-0.0866025403784438,-0.64,-0.15));
#25345=CARTESIAN_POINT('Origin',(-0.0866025403784439,-0.4,0.15));
#25346=CARTESIAN_POINT('',(-0.0866025403784439,-0.4,0.15));
#25347=CARTESIAN_POINT('',(-0.173205080756888,-0.4,-2.12115047744981E-17));
#25348=CARTESIAN_POINT('',(-0.0866025403784439,-0.64,0.15));
#25349=CARTESIAN_POINT('',(-0.0866025403784439,-0.4,0.15));
#25350=CARTESIAN_POINT('',(-0.173205080756888,-0.64,-2.12115047744981E-17));
#25351=CARTESIAN_POINT('Origin',(0.0866025403784439,-0.4,0.15));
#25352=CARTESIAN_POINT('',(0.0866025403784439,-0.4,0.15));
#25353=CARTESIAN_POINT('',(-0.0866025403784439,-0.4,0.15));
#25354=CARTESIAN_POINT('',(0.0866025403784439,-0.64,0.15));
#25355=CARTESIAN_POINT('',(0.0866025403784439,-0.4,0.15));
#25356=CARTESIAN_POINT('',(-0.0866025403784439,-0.64,0.15));
#25357=CARTESIAN_POINT('Origin',(0.173205080756888,-0.4,0.));
#25358=CARTESIAN_POINT('',(0.0866025403784439,-0.4,0.15));
#25359=CARTESIAN_POINT('',(0.0866025403784439,-0.64,0.15));
#25360=CARTESIAN_POINT('Origin',(0.,-0.4,-2.77555756156289E-17));
#25361=CARTESIAN_POINT('Origin',(0.,-0.64,-2.77555756156289E-17));
#73270=UNCERTAINTY_MEASURE_WITH_UNIT(LENGTH_MEASURE(0.001),#73367,
'DISTANCE_ACCURACY_VALUE',
'Maximum model space distance between geometric entities at asserted c
onnectivities');
#73302=UNCERTAINTY_MEASURE_WITH_UNIT(LENGTH_MEASURE(0.001),#73367,
'DISTANCE_ACCURACY_VALUE',
'Maximum model space distance between geometric entities at asserted c
onnectivities');
#73334=(
GEOMETRIC_REPRESENTATION_CONTEXT(3)
GLOBAL_UNCERTAINTY_ASSIGNED_CONTEXT((#73270))
GLOBAL_UNIT_ASSIGNED_CONTEXT((#73367,#73369,#73370))
REPRESENTATION_CONTEXT('','3D')
);
#73366=(
GEOMETRIC_REPRESENTATION_CONTEXT(3)
GLOBAL_UNCERTAINTY_ASSIGNED_CONTEXT((#73302))
GLOBAL_UNIT_ASSIGNED_CONTEXT((#73367,#73369,#73370))
REPRESENTATION_CONTEXT('','3D')
);
#73367=(
LENGTH_UNIT()
NAMED_UNIT(*)
SI_UNIT(.CENTI.,.METRE.)
);
#73369=(
NAMED_UNIT(*)
PLANE_ANGLE_UNIT()
SI_UNIT($,.RADIAN.)
);
#73370=(
NAMED_UNIT(*)
SI_UNIT($,.STERADIAN.)
SOLID_ANGLE_UNIT()
);
#73402=SHAPE_DEFINITION_REPRESENTATION(#73475,#73638);
#73475=PRODUCT_DEFINITION_SHAPE('',$,#73702);
#73638=SHAPE_REPRESENTATION('',(#17678),#73334);
#73670=PRODUCT_DEFINITION_CONTEXT('part definition',#73861,'design');
#73702=PRODUCT_DEFINITION('Cap Screw - M4x16','Cap Screw - M4x16',#73765,
#73670);
#73765=PRODUCT_DEFINITION_FORMATION('',$,#73894);
#73861=APPLICATION_CONTEXT(
'Core Data for Automotive Mechanical Design Process');
#73862=PRODUCT_CONTEXT('part definition',#73861,'mechanical');
#73894=PRODUCT('Cap Screw - M4x16','Cap Screw - M4x16',
'Cap Screw - M4x16',(#73862));
#73989=COLOUR_RGB('Black',0.12,0.14,0.17);
#73990=FILL_AREA_STYLE_COLOUR('',#73989);
#73991=FILL_AREA_STYLE('',(#73990));
#73992=SURFACE_STYLE_FILL_AREA(#73991);
#73993=SURFACE_SIDE_STYLE('',(#73992));
#73994=SURFACE_STYLE_USAGE(.BOTH.,#73993);
#73995=PRESENTATION_STYLE_ASSIGNMENT((#73994));
ENDSEC;
END-ISO-10303-21;
